ISO-10303-21;
HEADER;
/* Generated by software containing ST-Developer
 * from STEP Tools, Inc. (www.steptools.com) 
 */

FILE_DESCRIPTION(
/* description */ ('Bearing friction torque test rig'),
/* implementation_level */ '2;1');

FILE_NAME(
/* name */ 'Support cap (2).step',
/* time_stamp */ '2026-10-28T03:24:04-07:00',
/* author */ (''),
/* organization */ (''),
/* preprocessor_version */ 'ST-DEVELOPER v20.2',
/* originating_system */ 'Autodesk Translation Framework v15.17.0.0',
/* authorisation */ '');

FILE_SCHEMA (('AUTOMOTIVE_DESIGN { 1 0 10303 214 3 1 1 }'));
ENDSEC;

DATA;
#10=MECHANICAL_DESIGN_GEOMETRIC_PRESENTATION_REPRESENTATION('',(#544),#14822);
#466=SHAPE_REPRESENTATION_RELATIONSHIP('SRR','None',#15005,#505);
#505=ADVANCED_BREP_SHAPE_REPRESENTATION('',(#598),#14785);
#544=STYLED_ITEM('',(#15277),#598);
#598=MANIFOLD_SOLID_BREP('Body1',#7660);
#722=FACE_BOUND('',#1708,.T.);
#723=FACE_BOUND('',#1712,.T.);
#724=FACE_BOUND('',#1713,.T.);
#725=FACE_BOUND('',#1714,.T.);
#726=FACE_BOUND('',#1715,.T.);
#727=FACE_BOUND('',#1716,.T.);
#728=FACE_BOUND('',#1718,.T.);
#729=FACE_BOUND('',#1719,.T.);
#730=FACE_BOUND('',#1720,.T.);
#731=FACE_BOUND('',#1721,.T.);
#732=FACE_BOUND('',#1722,.T.);
#908=PLANE('',#8345);
#909=PLANE('',#8352);
#910=PLANE('',#8353);
#1179=FACE_OUTER_BOUND('',#1702,.T.);
#1180=FACE_OUTER_BOUND('',#1703,.T.);
#1181=FACE_OUTER_BOUND('',#1704,.T.);
#1182=FACE_OUTER_BOUND('',#1705,.T.);
#1183=FACE_OUTER_BOUND('',#1706,.T.);
#1184=FACE_OUTER_BOUND('',#1707,.T.);
#1185=FACE_OUTER_BOUND('',#1709,.T.);
#1186=FACE_OUTER_BOUND('',#1710,.T.);
#1187=FACE_OUTER_BOUND('',#1711,.T.);
#1188=FACE_OUTER_BOUND('',#1717,.T.);
#1702=EDGE_LOOP('',(#5532,#5533,#5534,#5535));
#1703=EDGE_LOOP('',(#5536,#5537,#5538,#5539));
#1704=EDGE_LOOP('',(#5540,#5541,#5542,#5543));
#1705=EDGE_LOOP('',(#5544,#5545,#5546,#5547));
#1706=EDGE_LOOP('',(#5548,#5549,#5550,#5551));
#1707=EDGE_LOOP('',(#5552));
#1708=EDGE_LOOP('',(#5553));
#1709=EDGE_LOOP('',(#5554,#5555,#5556,#5557));
#1710=EDGE_LOOP('',(#5558,#5559,#5560,#5561));
#1711=EDGE_LOOP('',(#5562));
#1712=EDGE_LOOP('',(#5563));
#1713=EDGE_LOOP('',(#5564));
#1714=EDGE_LOOP('',(#5565));
#1715=EDGE_LOOP('',(#5566));
#1716=EDGE_LOOP('',(#5567));
#1717=EDGE_LOOP('',(#5568));
#1718=EDGE_LOOP('',(#5569));
#1719=EDGE_LOOP('',(#5570));
#1720=EDGE_LOOP('',(#5571));
#1721=EDGE_LOOP('',(#5572));
#1722=EDGE_LOOP('',(#5573));
#2311=LINE('',#12070,#2755);
#2312=LINE('',#12076,#2756);
#2313=LINE('',#12082,#2757);
#2314=LINE('',#12088,#2758);
#2315=LINE('',#12094,#2759);
#2316=LINE('',#12101,#2760);
#2317=LINE('',#12107,#2761);
#2755=VECTOR('',#9638,0.225);
#2756=VECTOR('',#9645,0.225);
#2757=VECTOR('',#9652,0.225);
#2758=VECTOR('',#9659,0.225);
#2759=VECTOR('',#9666,1.59);
#2760=VECTOR('',#9675,1.1);
#2761=VECTOR('',#9682,2.5);
#3201=CIRCLE('',#8331,0.225);
#3202=CIRCLE('',#8332,0.225);
#3203=CIRCLE('',#8334,0.225);
#3204=CIRCLE('',#8335,0.225);
#3205=CIRCLE('',#8337,0.225);
#3206=CIRCLE('',#8338,0.225);
#3207=CIRCLE('',#8340,0.225);
#3208=CIRCLE('',#8341,0.225);
#3209=CIRCLE('',#8343,1.59);
#3210=CIRCLE('',#8344,1.59);
#3211=CIRCLE('',#8346,1.1);
#3212=CIRCLE('',#8348,1.1);
#3213=CIRCLE('',#8350,2.5);
#3214=CIRCLE('',#8351,2.5);
#3681=VERTEX_POINT('',#12067);
#3682=VERTEX_POINT('',#12069);
#3683=VERTEX_POINT('',#12073);
#3684=VERTEX_POINT('',#12075);
#3685=VERTEX_POINT('',#12079);
#3686=VERTEX_POINT('',#12081);
#3687=VERTEX_POINT('',#12085);
#3688=VERTEX_POINT('',#12087);
#3689=VERTEX_POINT('',#12091);
#3690=VERTEX_POINT('',#12093);
#3691=VERTEX_POINT('',#12097);
#3692=VERTEX_POINT('',#12100);
#3693=VERTEX_POINT('',#12104);
#3694=VERTEX_POINT('',#12106);
#4392=EDGE_CURVE('',#3681,#3681,#3201,.T.);
#4393=EDGE_CURVE('',#3681,#3682,#2311,.T.);
#4394=EDGE_CURVE('',#3682,#3682,#3202,.T.);
#4395=EDGE_CURVE('',#3683,#3683,#3203,.T.);
#4396=EDGE_CURVE('',#3683,#3684,#2312,.T.);
#4397=EDGE_CURVE('',#3684,#3684,#3204,.T.);
#4398=EDGE_CURVE('',#3685,#3685,#3205,.T.);
#4399=EDGE_CURVE('',#3685,#3686,#2313,.T.);
#4400=EDGE_CURVE('',#3686,#3686,#3206,.T.);
#4401=EDGE_CURVE('',#3687,#3687,#3207,.T.);
#4402=EDGE_CURVE('',#3687,#3688,#2314,.T.);
#4403=EDGE_CURVE('',#3688,#3688,#3208,.T.);
#4404=EDGE_CURVE('',#3689,#3689,#3209,.T.);
#4405=EDGE_CURVE('',#3689,#3690,#2315,.T.);
#4406=EDGE_CURVE('',#3690,#3690,#3210,.T.);
#4407=EDGE_CURVE('',#3691,#3691,#3211,.T.);
#4408=EDGE_CURVE('',#3691,#3692,#2316,.T.);
#4409=EDGE_CURVE('',#3692,#3692,#3212,.T.);
#4410=EDGE_CURVE('',#3693,#3693,#3213,.T.);
#4411=EDGE_CURVE('',#3693,#3694,#2317,.T.);
#4412=EDGE_CURVE('',#3694,#3694,#3214,.T.);
#5532=ORIENTED_EDGE('',*,*,#4392,.F.);
#5533=ORIENTED_EDGE('',*,*,#4393,.T.);
#5534=ORIENTED_EDGE('',*,*,#4394,.F.);
#5535=ORIENTED_EDGE('',*,*,#4393,.F.);
#5536=ORIENTED_EDGE('',*,*,#4395,.F.);
#5537=ORIENTED_EDGE('',*,*,#4396,.T.);
#5538=ORIENTED_EDGE('',*,*,#4397,.F.);
#5539=ORIENTED_EDGE('',*,*,#4396,.F.);
#5540=ORIENTED_EDGE('',*,*,#4398,.F.);
#5541=ORIENTED_EDGE('',*,*,#4399,.T.);
#5542=ORIENTED_EDGE('',*,*,#4400,.F.);
#5543=ORIENTED_EDGE('',*,*,#4399,.F.);
#5544=ORIENTED_EDGE('',*,*,#4401,.F.);
#5545=ORIENTED_EDGE('',*,*,#4402,.T.);
#5546=ORIENTED_EDGE('',*,*,#4403,.F.);
#5547=ORIENTED_EDGE('',*,*,#4402,.F.);
#5548=ORIENTED_EDGE('',*,*,#4404,.F.);
#5549=ORIENTED_EDGE('',*,*,#4405,.T.);
#5550=ORIENTED_EDGE('',*,*,#4406,.F.);
#5551=ORIENTED_EDGE('',*,*,#4405,.F.);
#5552=ORIENTED_EDGE('',*,*,#4404,.T.);
#5553=ORIENTED_EDGE('',*,*,#4407,.T.);
#5554=ORIENTED_EDGE('',*,*,#4407,.F.);
#5555=ORIENTED_EDGE('',*,*,#4408,.T.);
#5556=ORIENTED_EDGE('',*,*,#4409,.T.);
#5557=ORIENTED_EDGE('',*,*,#4408,.F.);
#5558=ORIENTED_EDGE('',*,*,#4410,.F.);
#5559=ORIENTED_EDGE('',*,*,#4411,.T.);
#5560=ORIENTED_EDGE('',*,*,#4412,.T.);
#5561=ORIENTED_EDGE('',*,*,#4411,.F.);
#5562=ORIENTED_EDGE('',*,*,#4410,.T.);
#5563=ORIENTED_EDGE('',*,*,#4406,.T.);
#5564=ORIENTED_EDGE('',*,*,#4403,.T.);
#5565=ORIENTED_EDGE('',*,*,#4400,.T.);
#5566=ORIENTED_EDGE('',*,*,#4397,.T.);
#5567=ORIENTED_EDGE('',*,*,#4394,.T.);
#5568=ORIENTED_EDGE('',*,*,#4412,.F.);
#5569=ORIENTED_EDGE('',*,*,#4409,.F.);
#5570=ORIENTED_EDGE('',*,*,#4401,.T.);
#5571=ORIENTED_EDGE('',*,*,#4398,.T.);
#5572=ORIENTED_EDGE('',*,*,#4395,.T.);
#5573=ORIENTED_EDGE('',*,*,#4392,.T.);
#7090=CYLINDRICAL_SURFACE('',#8330,0.225);
#7091=CYLINDRICAL_SURFACE('',#8333,0.225);
#7092=CYLINDRICAL_SURFACE('',#8336,0.225);
#7093=CYLINDRICAL_SURFACE('',#8339,0.225);
#7094=CYLINDRICAL_SURFACE('',#8342,1.59);
#7095=CYLINDRICAL_SURFACE('',#8347,1.1);
#7096=CYLINDRICAL_SURFACE('',#8349,2.5);
#7290=ADVANCED_FACE('',(#1179),#7090,.F.);
#7291=ADVANCED_FACE('',(#1180),#7091,.F.);
#7292=ADVANCED_FACE('',(#1181),#7092,.F.);
#7293=ADVANCED_FACE('',(#1182),#7093,.F.);
#7294=ADVANCED_FACE('',(#1183),#7094,.T.);
#7295=ADVANCED_FACE('',(#1184,#722),#908,.T.);
#7296=ADVANCED_FACE('',(#1185),#7095,.F.);
#7297=ADVANCED_FACE('',(#1186),#7096,.T.);
#7298=ADVANCED_FACE('',(#1187,#723,#724,#725,#726,#727),#909,.T.);
#7299=ADVANCED_FACE('',(#1188,#728,#729,#730,#731,#732),#910,.F.);
#7660=CLOSED_SHELL('',(#7290,#7291,#7292,#7293,#7294,#7295,#7296,#7297,
#7298,#7299));
#8329=AXIS2_PLACEMENT_3D('',#12065,#9632,#9633);
#8330=AXIS2_PLACEMENT_3D('',#12066,#9634,#9635);
#8331=AXIS2_PLACEMENT_3D('',#12068,#9636,#9637);
#8332=AXIS2_PLACEMENT_3D('',#12071,#9639,#9640);
#8333=AXIS2_PLACEMENT_3D('',#12072,#9641,#9642);
#8334=AXIS2_PLACEMENT_3D('',#12074,#9643,#9644);
#8335=AXIS2_PLACEMENT_3D('',#12077,#9646,#9647);
#8336=AXIS2_PLACEMENT_3D('',#12078,#9648,#9649);
#8337=AXIS2_PLACEMENT_3D('',#12080,#9650,#9651);
#8338=AXIS2_PLACEMENT_3D('',#12083,#9653,#9654);
#8339=AXIS2_PLACEMENT_3D('',#12084,#9655,#9656);
#8340=AXIS2_PLACEMENT_3D('',#12086,#9657,#9658);
#8341=AXIS2_PLACEMENT_3D('',#12089,#9660,#9661);
#8342=AXIS2_PLACEMENT_3D('',#12090,#9662,#9663);
#8343=AXIS2_PLACEMENT_3D('',#12092,#9664,#9665);
#8344=AXIS2_PLACEMENT_3D('',#12095,#9667,#9668);
#8345=AXIS2_PLACEMENT_3D('',#12096,#9669,#9670);
#8346=AXIS2_PLACEMENT_3D('',#12098,#9671,#9672);
#8347=AXIS2_PLACEMENT_3D('',#12099,#9673,#9674);
#8348=AXIS2_PLACEMENT_3D('',#12102,#9676,#9677);
#8349=AXIS2_PLACEMENT_3D('',#12103,#9678,#9679);
#8350=AXIS2_PLACEMENT_3D('',#12105,#9680,#9681);
#8351=AXIS2_PLACEMENT_3D('',#12108,#9683,#9684);
#8352=AXIS2_PLACEMENT_3D('',#12109,#9685,#9686);
#8353=AXIS2_PLACEMENT_3D('',#12110,#9687,#9688);
#9632=DIRECTION('axis',(0.,0.,1.));
#9633=DIRECTION('refdir',(1.,0.,0.));
#9634=DIRECTION('center_axis',(0.,1.,0.));
#9635=DIRECTION('ref_axis',(1.,0.,0.));
#9636=DIRECTION('center_axis',(0.,1.,0.));
#9637=DIRECTION('ref_axis',(1.,0.,0.));
#9638=DIRECTION('',(0.,1.,0.));
#9639=DIRECTION('center_axis',(0.,-1.,0.));
#9640=DIRECTION('ref_axis',(1.,0.,0.));
#9641=DIRECTION('center_axis',(0.,1.,0.));
#9642=DIRECTION('ref_axis',(1.,0.,0.));
#9643=DIRECTION('center_axis',(0.,1.,0.));
#9644=DIRECTION('ref_axis',(1.,0.,0.));
#9645=DIRECTION('',(0.,1.,0.));
#9646=DIRECTION('center_axis',(0.,-1.,0.));
#9647=DIRECTION('ref_axis',(1.,0.,0.));
#9648=DIRECTION('center_axis',(0.,1.,0.));
#9649=DIRECTION('ref_axis',(1.,0.,0.));
#9650=DIRECTION('center_axis',(0.,1.,0.));
#9651=DIRECTION('ref_axis',(1.,0.,0.));
#9652=DIRECTION('',(0.,1.,0.));
#9653=DIRECTION('center_axis',(0.,-1.,0.));
#9654=DIRECTION('ref_axis',(1.,0.,0.));
#9655=DIRECTION('center_axis',(0.,1.,0.));
#9656=DIRECTION('ref_axis',(1.,0.,0.));
#9657=DIRECTION('center_axis',(0.,1.,0.));
#9658=DIRECTION('ref_axis',(1.,0.,0.));
#9659=DIRECTION('',(0.,1.,0.));
#9660=DIRECTION('center_axis',(0.,-1.,0.));
#9661=DIRECTION('ref_axis',(1.,0.,0.));
#9662=DIRECTION('center_axis',(0.,1.,0.));
#9663=DIRECTION('ref_axis',(1.,0.,0.));
#9664=DIRECTION('center_axis',(0.,1.,0.));
#9665=DIRECTION('ref_axis',(1.,0.,0.));
#9666=DIRECTION('',(0.,-1.,0.));
#9667=DIRECTION('center_axis',(0.,-1.,0.));
#9668=DIRECTION('ref_axis',(1.,0.,0.));
#9669=DIRECTION('center_axis',(0.,1.,0.));
#9670=DIRECTION('ref_axis',(1.,0.,0.));
#9671=DIRECTION('center_axis',(0.,-1.,0.));
#9672=DIRECTION('ref_axis',(1.,0.,0.));
#9673=DIRECTION('center_axis',(0.,1.,0.));
#9674=DIRECTION('ref_axis',(1.,0.,0.));
#9675=DIRECTION('',(0.,-1.,0.));
#9676=DIRECTION('center_axis',(0.,-1.,0.));
#9677=DIRECTION('ref_axis',(1.,0.,0.));
#9678=DIRECTION('center_axis',(0.,1.,0.));
#9679=DIRECTION('ref_axis',(1.,0.,0.));
#9680=DIRECTION('center_axis',(0.,1.,0.));
#9681=DIRECTION('ref_axis',(1.,0.,0.));
#9682=DIRECTION('',(0.,-1.,0.));
#9683=DIRECTION('center_axis',(0.,1.,0.));
#9684=DIRECTION('ref_axis',(1.,0.,0.));
#9685=DIRECTION('center_axis',(0.,1.,0.));
#9686=DIRECTION('ref_axis',(1.,0.,0.));
#9687=DIRECTION('center_axis',(0.,1.,0.));
#9688=DIRECTION('ref_axis',(1.,0.,0.));
#12065=CARTESIAN_POINT('',(0.,0.,0.));
#12066=CARTESIAN_POINT('Origin',(-2.,5.8,7.));
#12067=CARTESIAN_POINT('',(-2.225,5.9,7.));
#12068=CARTESIAN_POINT('Origin',(-2.,5.9,7.));
#12069=CARTESIAN_POINT('',(-2.225,6.2,7.));
#12070=CARTESIAN_POINT('',(-2.225,5.8,7.));
#12071=CARTESIAN_POINT('Origin',(-2.,6.2,7.));
#12072=CARTESIAN_POINT('Origin',(1.22464679914735E-16,5.8,9.));
#12073=CARTESIAN_POINT('',(-0.225,5.9,9.));
#12074=CARTESIAN_POINT('Origin',(1.22464679914735E-16,5.9,9.));
#12075=CARTESIAN_POINT('',(-0.225,6.2,9.));
#12076=CARTESIAN_POINT('',(-0.225,5.8,9.));
#12077=CARTESIAN_POINT('Origin',(1.22464679914735E-16,6.2,9.));
#12078=CARTESIAN_POINT('Origin',(2.,5.8,7.));
#12079=CARTESIAN_POINT('',(1.775,5.9,7.));
#12080=CARTESIAN_POINT('Origin',(2.,5.9,7.));
#12081=CARTESIAN_POINT('',(1.775,6.2,7.));
#12082=CARTESIAN_POINT('',(1.775,5.8,7.));
#12083=CARTESIAN_POINT('Origin',(2.,6.2,7.));
#12084=CARTESIAN_POINT('Origin',(-3.67394039744206E-16,5.8,5.));
#12085=CARTESIAN_POINT('',(-0.225,5.9,5.));
#12086=CARTESIAN_POINT('Origin',(-3.67394039744206E-16,5.9,5.));
#12087=CARTESIAN_POINT('',(-0.225,6.2,5.));
#12088=CARTESIAN_POINT('',(-0.225,5.8,5.));
#12089=CARTESIAN_POINT('Origin',(-3.67394039744206E-16,6.2,5.));
#12090=CARTESIAN_POINT('Origin',(0.,6.2,7.));
#12091=CARTESIAN_POINT('',(-1.59,6.5,7.));
#12092=CARTESIAN_POINT('Origin',(0.,6.5,7.));
#12093=CARTESIAN_POINT('',(-1.59,6.2,7.));
#12094=CARTESIAN_POINT('',(-1.59,6.2,7.));
#12095=CARTESIAN_POINT('Origin',(0.,6.2,7.));
#12096=CARTESIAN_POINT('Origin',(0.,6.5,7.));
#12097=CARTESIAN_POINT('',(-1.1,6.5,7.));
#12098=CARTESIAN_POINT('Origin',(0.,6.5,7.));
#12099=CARTESIAN_POINT('Origin',(0.,5.9,7.));
#12100=CARTESIAN_POINT('',(-1.1,5.9,7.));
#12101=CARTESIAN_POINT('',(-1.1,5.9,7.));
#12102=CARTESIAN_POINT('Origin',(0.,5.9,7.));
#12103=CARTESIAN_POINT('Origin',(0.,5.9,7.));
#12104=CARTESIAN_POINT('',(-2.5,6.2,7.));
#12105=CARTESIAN_POINT('Origin',(0.,6.2,7.));
#12106=CARTESIAN_POINT('',(-2.5,5.9,7.));
#12107=CARTESIAN_POINT('',(-2.5,5.9,7.));
#12108=CARTESIAN_POINT('Origin',(0.,5.9,7.));
#12109=CARTESIAN_POINT('Origin',(0.,6.2,7.));
#12110=CARTESIAN_POINT('Origin',(0.,5.9,7.));
#14740=UNCERTAINTY_MEASURE_WITH_UNIT(LENGTH_MEASURE(0.001),#14823,
'DISTANCE_ACCURACY_VALUE',
'Maximum model space distance between geometric entities at asserted c
onnectivities');
#14777=UNCERTAINTY_MEASURE_WITH_UNIT(LENGTH_MEASURE(0.001),#14823,
'DISTANCE_ACCURACY_VALUE',
'Maximum model space distance between geometric entities at asserted c
onnectivities');
#14785=(
GEOMETRIC_REPRESENTATION_CONTEXT(3)
GLOBAL_UNCERTAINTY_ASSIGNED_CONTEXT((#14740))
GLOBAL_UNIT_ASSIGNED_CONTEXT((#14823,#14825,#14826))
REPRESENTATION_CONTEXT('','3D')
);
#14822=(
GEOMETRIC_REPRESENTATION_CONTEXT(3)
GLOBAL_UNCERTAINTY_ASSIGNED_CONTEXT((#14777))
GLOBAL_UNIT_ASSIGNED_CONTEXT((#14823,#14825,#14826))
REPRESENTATION_CONTEXT('','3D')
);
#14823=(
LENGTH_UNIT()
NAMED_UNIT(*)
SI_UNIT(.CENTI.,.METRE.)
);
#14825=(
NAMED_UNIT(*)
PLANE_ANGLE_UNIT()
SI_UNIT($,.RADIAN.)
);
#14826=(
NAMED_UNIT(*)
SI_UNIT($,.STERADIAN.)
SOLID_ANGLE_UNIT()
);
#14834=SHAPE_DEFINITION_REPRESENTATION(#14878,#15005);
#14878=PRODUCT_DEFINITION_SHAPE('',$,#15050);
#15005=SHAPE_REPRESENTATION('',(#8329),#14785);
#15042=PRODUCT_DEFINITION_CONTEXT('part definition',#15176,'design');
#15050=PRODUCT_DEFINITION('Support cap (2)','Support cap (2)',#15094,#15042);
#15094=PRODUCT_DEFINITION_FORMATION('',$,#15185);
#15176=APPLICATION_CONTEXT(
'Core Data for Automotive Mechanical Design Process');
#15177=PRODUCT_CONTEXT('part definition',#15176,'mechanical');
#15185=PRODUCT('Support cap (2)','Support cap (2)','Support cap (2)',(#15177));
#15271=COLOUR_RGB('Sky Blue',0.24,0.69,0.87);
#15272=FILL_AREA_STYLE_COLOUR('',#15271);
#15273=FILL_AREA_STYLE('',(#15272));
#15274=SURFACE_STYLE_FILL_AREA(#15273);
#15275=SURFACE_SIDE_STYLE('',(#15274));
#15276=SURFACE_STYLE_USAGE(.BOTH.,#15275);
#15277=PRESENTATION_STYLE_ASSIGNMENT((#15276));
ENDSEC;
END-ISO-10303-21;
